ISO-10303-21;
HEADER;
/* Generated by software containing ST-Developer
 * from STEP Tools, Inc. (www.steptools.com) 
 */

FILE_DESCRIPTION(
/* description */ ('Dual-rail gantry carriage'),
/* implementation_level */ '2;1');

FILE_NAME(
/* name */ 'Cap Screw - M4x16.step',
/* time_stamp */ '2026-10-27T10:49:15-07:00',
/* author */ (''),
/* organization */ (''),
/* preprocessor_version */ 'ST-DEVELOPER v20.2',
/* originating_system */ 'Autodesk Translation Framework v15.17.0.0',
/* authorisation */ '');

FILE_SCHEMA (('AUTOMOTIVE_DESIGN { 1 0 10303 214 3 1 1 }'));
ENDSEC;

DATA;
#10=MECHANICAL_DESIGN_GEOMETRIC_PRESENTATION_REPRESENTATION('',(#601),#12804);
#493=ORIENTED_CLOSED_SHELL('',*,#7380,.F.);
#498=CONICAL_SURFACE('',#8041,0.325,0.785398163397448);
#499=CONICAL_SURFACE('',#8045,0.335,0.785398163397448);
#500=CONICAL_SURFACE('',#8049,0.21,0.463647609000806);
#501=CONICAL_SURFACE('',#8053,0.18,0.785398163397448);
#518=BREP_WITH_VOIDS('Body1',#7379,(#493));
#539=SHAPE_REPRESENTATION_RELATIONSHIP('SRR','None',#13017,#570);
#570=ADVANCED_BREP_SHAPE_REPRESENTATION('',(#518),#12787);
#601=STYLED_ITEM('',(#13254),#518);
#704=FACE_BOUND('',#1701,.T.);
#920=PLANE('',#8039);
#921=PLANE('',#8047);
#922=PLANE('',#8055);
#923=PLANE('',#8056);
#924=PLANE('',#8057);
#925=PLANE('',#8058);
#926=PLANE('',#8059);
#927=PLANE('',#8060);
#928=PLANE('',#8061);
#929=PLANE('',#8062);
#930=PLANE('',#8063);
#1245=FACE_OUTER_BOUND('',#1696,.T.);
#1246=FACE_OUTER_BOUND('',#1697,.T.);
#1247=FACE_OUTER_BOUND('',#1698,.T.);
#1248=FACE_OUTER_BOUND('',#1699,.T.);
#1249=FACE_OUTER_BOUND('',#1700,.T.);
#1250=FACE_OUTER_BOUND('',#1702,.T.);
#1251=FACE_OUTER_BOUND('',#1703,.T.);
#1252=FACE_OUTER_BOUND('',#1704,.T.);
#1253=FACE_OUTER_BOUND('',#1705,.T.);
#1254=FACE_OUTER_BOUND('',#1706,.T.);
#1255=FACE_OUTER_BOUND('',#1707,.T.);
#1256=FACE_OUTER_BOUND('',#1708,.T.);
#1257=FACE_OUTER_BOUND('',#1709,.T.);
#1258=FACE_OUTER_BOUND('',#1710,.T.);
#1259=FACE_OUTER_BOUND('',#1711,.T.);
#1260=FACE_OUTER_BOUND('',#1712,.T.);
#1261=FACE_OUTER_BOUND('',#1713,.T.);
#1696=EDGE_LOOP('',(#6017));
#1697=EDGE_LOOP('',(#6018,#6019,#6020,#6021));
#1698=EDGE_LOOP('',(#6022,#6023,#6024,#6025));
#1699=EDGE_LOOP('',(#6026,#6027,#6028,#6029));
#1700=EDGE_LOOP('',(#6030));
#1701=EDGE_LOOP('',(#6031));
#1702=EDGE_LOOP('',(#6032,#6033,#6034,#6035));
#1703=EDGE_LOOP('',(#6036,#6037,#6038,#6039));
#1704=EDGE_LOOP('',(#6040,#6041,#6042,#6043));
#1705=EDGE_LOOP('',(#6044));
#1706=EDGE_LOOP('',(#6045,#6046,#6047,#6048));
#1707=EDGE_LOOP('',(#6049,#6050,#6051,#6052));
#1708=EDGE_LOOP('',(#6053,#6054,#6055,#6056));
#1709=EDGE_LOOP('',(#6057,#6058,#6059,#6060));
#1710=EDGE_LOOP('',(#6061,#6062,#6063,#6064));
#1711=EDGE_LOOP('',(#6065,#6066,#6067,#6068));
#1712=EDGE_LOOP('',(#6069,#6070,#6071,#6072,#6073,#6074));
#1713=EDGE_LOOP('',(#6075,#6076,#6077,#6078,#6079,#6080));
#2341=LINE('',#11691,#3050);
#2342=LINE('',#11695,#3051);
#2343=LINE('',#11699,#3052);
#2344=LINE('',#11706,#3053);
#2345=LINE('',#11710,#3054);
#2346=LINE('',#11714,#3055);
#2347=LINE('',#11719,#3056);
#2348=LINE('',#11721,#3057);
#2349=LINE('',#11723,#3058);
#2350=LINE('',#11724,#3059);
#2351=LINE('',#11727,#3060);
#2352=LINE('',#11729,#3061);
#2353=LINE('',#11730,#3062);
#2354=LINE('',#11733,#3063);
#2355=LINE('',#11735,#3064);
#2356=LINE('',#11736,#3065);
#2357=LINE('',#11739,#3066);
#2358=LINE('',#11741,#3067);
#2359=LINE('',#11742,#3068);
#2360=LINE('',#11745,#3069);
#2361=LINE('',#11747,#3070);
#2362=LINE('',#11748,#3071);
#2363=LINE('',#11750,#3072);
#2364=LINE('',#11751,#3073);
#3050=VECTOR('',#9484,0.325);
#3051=VECTOR('',#9489,0.35);
#3052=VECTOR('',#9494,0.335);
#3053=VECTOR('',#9503,0.21);
#3054=VECTOR('',#9508,0.2);
#3055=VECTOR('',#9513,0.18);
#3056=VECTOR('',#9518,1.);
#3057=VECTOR('',#9519,1.);
#3058=VECTOR('',#9520,1.);
#3059=VECTOR('',#9521,1.);
#3060=VECTOR('',#9524,1.);
#3061=VECTOR('',#9525,1.);
#3062=VECTOR('',#9526,1.);
#3063=VECTOR('',#9529,1.);
#3064=VECTOR('',#9530,1.);
#3065=VECTOR('',#9531,1.);
#3066=VECTOR('',#9534,1.);
#3067=VECTOR('',#9535,1.);
#3068=VECTOR('',#9536,1.);
#3069=VECTOR('',#9539,1.);
#3070=VECTOR('',#9540,1.);
#3071=VECTOR('',#9541,1.);
#3072=VECTOR('',#9544,1.);
#3073=VECTOR('',#9545,1.);
#3448=CIRCLE('',#8040,0.3);
#3449=CIRCLE('',#8042,0.35);
#3450=CIRCLE('',#8044,0.35);
#3451=CIRCLE('',#8046,0.32);
#3452=CIRCLE('',#8048,0.22);
#3453=CIRCLE('',#8050,0.1954);
#3454=CIRCLE('',#8052,0.1954);
#3455=CIRCLE('',#8054,0.16);
#3872=VERTEX_POINT('',#11686);
#3873=VERTEX_POINT('',#11689);
#3874=VERTEX_POINT('',#11693);
#3875=VERTEX_POINT('',#11697);
#3876=VERTEX_POINT('',#11701);
#3877=VERTEX_POINT('',#11704);
#3878=VERTEX_POINT('',#11708);
#3879=VERTEX_POINT('',#11712);
#3880=VERTEX_POINT('',#11717);
#3881=VERTEX_POINT('',#11718);
#3882=VERTEX_POINT('',#11720);
#3883=VERTEX_POINT('',#11722);
#3884=VERTEX_POINT('',#11726);
#3885=VERTEX_POINT('',#11728);
#3886=VERTEX_POINT('',#11732);
#3887=VERTEX_POINT('',#11734);
#3888=VERTEX_POINT('',#11738);
#3889=VERTEX_POINT('',#11740);
#3890=VERTEX_POINT('',#11744);
#3891=VERTEX_POINT('',#11746);
#4631=EDGE_CURVE('',#3872,#3872,#3448,.T.);
#4632=EDGE_CURVE('',#3873,#3873,#3449,.T.);
#4633=EDGE_CURVE('',#3873,#3872,#2341,.T.);
#4634=EDGE_CURVE('',#3874,#3874,#3450,.T.);
#4635=EDGE_CURVE('',#3874,#3873,#2342,.T.);
#4636=EDGE_CURVE('',#3875,#3875,#3451,.T.);
#4637=EDGE_CURVE('',#3875,#3874,#2343,.T.);
#4638=EDGE_CURVE('',#3876,#3876,#3452,.T.);
#4639=EDGE_CURVE('',#3877,#3877,#3453,.F.);
#4640=EDGE_CURVE('',#3877,#3876,#2344,.T.);
#4641=EDGE_CURVE('',#3878,#3878,#3454,.F.);
#4642=EDGE_CURVE('',#3878,#3877,#2345,.T.);
#4643=EDGE_CURVE('',#3879,#3879,#3455,.T.);
#4644=EDGE_CURVE('',#3879,#3878,#2346,.T.);
#4645=EDGE_CURVE('',#3880,#3881,#2347,.T.);
#4646=EDGE_CURVE('',#3881,#3882,#2348,.T.);
#4647=EDGE_CURVE('',#3882,#3883,#2349,.T.);
#4648=EDGE_CURVE('',#3880,#3883,#2350,.T.);
#4649=EDGE_CURVE('',#3881,#3884,#2351,.T.);
#4650=EDGE_CURVE('',#3884,#3885,#2352,.T.);
#4651=EDGE_CURVE('',#3885,#3882,#2353,.T.);
#4652=EDGE_CURVE('',#3884,#3886,#2354,.T.);
#4653=EDGE_CURVE('',#3886,#3887,#2355,.T.);
#4654=EDGE_CURVE('',#3887,#3885,#2356,.T.);
#4655=EDGE_CURVE('',#3886,#3888,#2357,.T.);
#4656=EDGE_CURVE('',#3888,#3889,#2358,.T.);
#4657=EDGE_CURVE('',#3889,#3887,#2359,.T.);
#4658=EDGE_CURVE('',#3888,#3890,#2360,.T.);
#4659=EDGE_CURVE('',#3890,#3891,#2361,.T.);
#4660=EDGE_CURVE('',#3891,#3889,#2362,.T.);
#4661=EDGE_CURVE('',#3890,#3880,#2363,.T.);
#4662=EDGE_CURVE('',#3883,#3891,#2364,.T.);
#6017=ORIENTED_EDGE('',*,*,#4631,.F.);
#6018=ORIENTED_EDGE('',*,*,#4632,.F.);
#6019=ORIENTED_EDGE('',*,*,#4633,.T.);
#6020=ORIENTED_EDGE('',*,*,#4631,.T.);
#6021=ORIENTED_EDGE('',*,*,#4633,.F.);
#6022=ORIENTED_EDGE('',*,*,#4634,.F.);
#6023=ORIENTED_EDGE('',*,*,#4635,.T.);
#6024=ORIENTED_EDGE('',*,*,#4632,.T.);
#6025=ORIENTED_EDGE('',*,*,#4635,.F.);
#6026=ORIENTED_EDGE('',*,*,#4636,.F.);
#6027=ORIENTED_EDGE('',*,*,#4637,.T.);
#6028=ORIENTED_EDGE('',*,*,#4634,.T.);
#6029=ORIENTED_EDGE('',*,*,#4637,.F.);
#6030=ORIENTED_EDGE('',*,*,#4636,.T.);
#6031=ORIENTED_EDGE('',*,*,#4638,.F.);
#6032=ORIENTED_EDGE('',*,*,#4639,.F.);
#6033=ORIENTED_EDGE('',*,*,#4640,.T.);
#6034=ORIENTED_EDGE('',*,*,#4638,.T.);
#6035=ORIENTED_EDGE('',*,*,#4640,.F.);
#6036=ORIENTED_EDGE('',*,*,#4641,.F.);
#6037=ORIENTED_EDGE('',*,*,#4642,.T.);
#6038=ORIENTED_EDGE('',*,*,#4639,.T.);
#6039=ORIENTED_EDGE('',*,*,#4642,.F.);
#6040=ORIENTED_EDGE('',*,*,#4643,.F.);
#6041=ORIENTED_EDGE('',*,*,#4644,.T.);
#6042=ORIENTED_EDGE('',*,*,#4641,.T.);
#6043=ORIENTED_EDGE('',*,*,#4644,.F.);
#6044=ORIENTED_EDGE('',*,*,#4643,.T.);
#6045=ORIENTED_EDGE('',*,*,#4645,.T.);
#6046=ORIENTED_EDGE('',*,*,#4646,.T.);
#6047=ORIENTED_EDGE('',*,*,#4647,.T.);
#6048=ORIENTED_EDGE('',*,*,#4648,.F.);
#6049=ORIENTED_EDGE('',*,*,#4649,.T.);
#6050=ORIENTED_EDGE('',*,*,#4650,.T.);
#6051=ORIENTED_EDGE('',*,*,#4651,.T.);
#6052=ORIENTED_EDGE('',*,*,#4646,.F.);
#6053=ORIENTED_EDGE('',*,*,#4652,.T.);
#6054=ORIENTED_EDGE('',*,*,#4653,.T.);
#6055=ORIENTED_EDGE('',*,*,#4654,.T.);
#6056=ORIENTED_EDGE('',*,*,#4650,.F.);
#6057=ORIENTED_EDGE('',*,*,#4655,.T.);
#6058=ORIENTED_EDGE('',*,*,#4656,.T.);
#6059=ORIENTED_EDGE('',*,*,#4657,.T.);
#6060=ORIENTED_EDGE('',*,*,#4653,.F.);
#6061=ORIENTED_EDGE('',*,*,#4658,.T.);
#6062=ORIENTED_EDGE('',*,*,#4659,.T.);
#6063=ORIENTED_EDGE('',*,*,#4660,.T.);
#6064=ORIENTED_EDGE('',*,*,#4656,.F.);
#6065=ORIENTED_EDGE('',*,*,#4661,.T.);
#6066=ORIENTED_EDGE('',*,*,#4648,.T.);
#6067=ORIENTED_EDGE('',*,*,#4662,.T.);
#6068=ORIENTED_EDGE('',*,*,#4659,.F.);
#6069=ORIENTED_EDGE('',*,*,#4661,.F.);
#6070=ORIENTED_EDGE('',*,*,#4658,.F.);
#6071=ORIENTED_EDGE('',*,*,#4655,.F.);
#6072=ORIENTED_EDGE('',*,*,#4652,.F.);
#6073=ORIENTED_EDGE('',*,*,#4649,.F.);
#6074=ORIENTED_EDGE('',*,*,#4645,.F.);
#6075=ORIENTED_EDGE('',*,*,#4662,.F.);
#6076=ORIENTED_EDGE('',*,*,#4647,.F.);
#6077=ORIENTED_EDGE('',*,*,#4651,.F.);
#6078=ORIENTED_EDGE('',*,*,#4654,.F.);
#6079=ORIENTED_EDGE('',*,*,#4657,.F.);
#6080=ORIENTED_EDGE('',*,*,#4660,.F.);
#6930=CYLINDRICAL_SURFACE('',#8043,0.35);
#6931=CYLINDRICAL_SURFACE('',#8051,0.1954);
#7171=ADVANCED_FACE('',(#1245),#920,.T.);
#7172=ADVANCED_FACE('',(#1246),#498,.T.);
#7173=ADVANCED_FACE('',(#1247),#6930,.T.);
#7174=ADVANCED_FACE('',(#1248),#499,.T.);
#7175=ADVANCED_FACE('',(#1249,#704),#921,.T.);
#7176=ADVANCED_FACE('',(#1250),#500,.T.);
#7177=ADVANCED_FACE('',(#1251),#6931,.T.);
#7178=ADVANCED_FACE('',(#1252),#501,.T.);
#7179=ADVANCED_FACE('',(#1253),#922,.T.);
#7180=ADVANCED_FACE('',(#1254),#923,.F.);
#7181=ADVANCED_FACE('',(#1255),#924,.F.);
#7182=ADVANCED_FACE('',(#1256),#925,.F.);
#7183=ADVANCED_FACE('',(#1257),#926,.F.);
#7184=ADVANCED_FACE('',(#1258),#927,.F.);
#7185=ADVANCED_FACE('',(#1259),#928,.F.);
#7186=ADVANCED_FACE('',(#1260),#929,.F.);
#7187=ADVANCED_FACE('',(#1261),#930,.F.);
#7379=CLOSED_SHELL('',(#7171,#7172,#7173,#7174,#7175,#7176,#7177,#7178,
#7179));
#7380=CLOSED_SHELL('',(#7180,#7181,#7182,#7183,#7184,#7185,#7186,#7187));
#8038=AXIS2_PLACEMENT_3D('',#11684,#9474,#9475);
#8039=AXIS2_PLACEMENT_3D('',#11685,#9476,#9477);
#8040=AXIS2_PLACEMENT_3D('',#11687,#9478,#9479);
#8041=AXIS2_PLACEMENT_3D('',#11688,#9480,#9481);
#8042=AXIS2_PLACEMENT_3D('',#11690,#9482,#9483);
#8043=AXIS2_PLACEMENT_3D('',#11692,#9485,#9486);
#8044=AXIS2_PLACEMENT_3D('',#11694,#9487,#9488);
#8045=AXIS2_PLACEMENT_3D('',#11696,#9490,#9491);
#8046=AXIS2_PLACEMENT_3D('',#11698,#9492,#9493);
#8047=AXIS2_PLACEMENT_3D('',#11700,#9495,#9496);
#8048=AXIS2_PLACEMENT_3D('',#11702,#9497,#9498);
#8049=AXIS2_PLACEMENT_3D('',#11703,#9499,#9500);
#8050=AXIS2_PLACEMENT_3D('',#11705,#9501,#9502);
#8051=AXIS2_PLACEMENT_3D('',#11707,#9504,#9505);
#8052=AXIS2_PLACEMENT_3D('',#11709,#9506,#9507);
#8053=AXIS2_PLACEMENT_3D('',#11711,#9509,#9510);
#8054=AXIS2_PLACEMENT_3D('',#11713,#9511,#9512);
#8055=AXIS2_PLACEMENT_3D('',#11715,#9514,#9515);
#8056=AXIS2_PLACEMENT_3D('',#11716,#9516,#9517);
#8057=AXIS2_PLACEMENT_3D('',#11725,#9522,#9523);
#8058=AXIS2_PLACEMENT_3D('',#11731,#9527,#9528);
#8059=AXIS2_PLACEMENT_3D('',#11737,#9532,#9533);
#8060=AXIS2_PLACEMENT_3D('',#11743,#9537,#9538);
#8061=AXIS2_PLACEMENT_3D('',#11749,#9542,#9543);
#8062=AXIS2_PLACEMENT_3D('',#11752,#9546,#9547);
#8063=AXIS2_PLACEMENT_3D('',#11753,#9548,#9549);
#9474=DIRECTION('axis',(0.,0.,1.));
#9475=DIRECTION('refdir',(1.,0.,0.));
#9476=DIRECTION('center_axis',(0.,1.,0.));
#9477=DIRECTION('ref_axis',(0.,0.,1.));
#9478=DIRECTION('center_axis',(0.,-1.,0.));
#9479=DIRECTION('ref_axis',(1.,0.,0.));
#9480=DIRECTION('center_axis',(0.,-1.,0.));
#9481=DIRECTION('ref_axis',(1.,0.,0.));
#9482=DIRECTION('center_axis',(0.,-1.,0.));
#9483=DIRECTION('ref_axis',(1.,0.,0.));
#9484=DIRECTION('',(0.707106781186547,0.707106781186548,8.65956056235493E-17));
#9485=DIRECTION('center_axis',(0.,-1.,0.));
#9486=DIRECTION('ref_axis',(1.,0.,0.));
#9487=DIRECTION('center_axis',(0.,-1.,0.));
#9488=DIRECTION('ref_axis',(1.,0.,0.));
#9489=DIRECTION('',(0.,1.,0.));
#9490=DIRECTION('center_axis',(0.,1.,0.));
#9491=DIRECTION('ref_axis',(1.,0.,0.));
#9492=DIRECTION('center_axis',(0.,-1.,0.));
#9493=DIRECTION('ref_axis',(1.,0.,0.));
#9494=DIRECTION('',(-0.707106781186547,0.707106781186548,-8.65956056235493E-17));
#9495=DIRECTION('center_axis',(0.,-1.,0.));
#9496=DIRECTION('ref_axis',(0.,0.,-1.));
#9497=DIRECTION('center_axis',(0.,-1.,0.));
#9498=DIRECTION('ref_axis',(1.,0.,0.));
#9499=DIRECTION('center_axis',(0.,1.,0.));
#9500=DIRECTION('ref_axis',(1.,0.,0.));
#9501=DIRECTION('center_axis',(0.,1.,0.));
#9502=DIRECTION('ref_axis',(1.,0.,0.));
#9503=DIRECTION('',(-0.447213595499958,0.894427190999916,-5.47678698264203E-17));
#9504=DIRECTION('center_axis',(0.,-1.,0.));
#9505=DIRECTION('ref_axis',(1.,0.,0.));
#9506=DIRECTION('center_axis',(0.,1.,0.));
#9507=DIRECTION('ref_axis',(1.,0.,0.));
#9508=DIRECTION('',(0.,1.,0.));
#9509=DIRECTION('center_axis',(0.,1.,0.));
#9510=DIRECTION('ref_axis',(1.,0.,0.));
#9511=DIRECTION('center_axis',(0.,-1.,0.));
#9512=DIRECTION('ref_axis',(1.,0.,0.));
#9513=DIRECTION('',(-0.707106781186547,0.707106781186548,-8.65956056235493E-17));
#9514=DIRECTION('center_axis',(0.,-1.,0.));
#9515=DIRECTION('ref_axis',(0.,0.,-1.));
#9516=DIRECTION('center_axis',(0.866025403784439,0.,-0.5));
#9517=DIRECTION('ref_axis',(0.5,0.,0.866025403784439));
#9518=DIRECTION('',(-0.5,0.,-0.866025403784439));
#9519=DIRECTION('',(0.,-1.,0.));
#9520=DIRECTION('',(0.5,0.,0.866025403784439));
#9521=DIRECTION('',(0.,-1.,0.));
#9522=DIRECTION('center_axis',(1.60246890531964E-16,0.,-1.));
#9523=DIRECTION('ref_axis',(1.,0.,1.60246890531964E-16));
#9524=DIRECTION('',(-1.,0.,-1.60246890531964E-16));
#9525=DIRECTION('',(0.,-1.,0.));
#9526=DIRECTION('',(1.,0.,1.60246890531964E-16));
#9527=DIRECTION('center_axis',(-0.866025403784439,0.,-0.5));
#9528=DIRECTION('ref_axis',(0.5,0.,-0.866025403784439));
#9529=DIRECTION('',(-0.5,0.,0.866025403784439));
#9530=DIRECTION('',(0.,-1.,0.));
#9531=DIRECTION('',(0.5,0.,-0.866025403784439));
#9532=DIRECTION('center_axis',(-0.866025403784439,0.,0.5));
#9533=DIRECTION('ref_axis',(-0.5,0.,-0.866025403784439));
#9534=DIRECTION('',(0.5,0.,0.866025403784439));
#9535=DIRECTION('',(0.,-1.,0.));
#9536=DIRECTION('',(-0.5,0.,-0.866025403784439));
#9537=DIRECTION('center_axis',(-1.60246890531964E-16,0.,1.));
#9538=DIRECTION('ref_axis',(-1.,0.,-1.60246890531964E-16));
#9539=DIRECTION('',(1.,0.,1.60246890531964E-16));
#9540=DIRECTION('',(0.,-1.,0.));
#9541=DIRECTION('',(-1.,0.,-1.60246890531964E-16));
#9542=DIRECTION('center_axis',(0.866025403784439,0.,0.5));
#9543=DIRECTION('ref_axis',(-0.5,0.,0.866025403784439));
#9544=DIRECTION('',(0.5,0.,-0.866025403784439));
#9545=DIRECTION('',(-0.5,0.,0.866025403784439));
#9546=DIRECTION('center_axis',(0.,1.,0.));
#9547=DIRECTION('ref_axis',(1.,0.,0.));
#9548=DIRECTION('center_axis',(0.,-1.,0.));
#9549=DIRECTION('ref_axis',(0.,0.,-1.));
#11684=CARTESIAN_POINT('',(0.,0.,0.));
#11685=CARTESIAN_POINT('Origin',(0.3,0.4,0.));
#11686=CARTESIAN_POINT('',(-0.3,0.4,-3.67394039744206E-17));
#11687=CARTESIAN_POINT('Origin',(0.,0.4,0.));
#11688=CARTESIAN_POINT('Origin',(0.,0.375,0.));
#11689=CARTESIAN_POINT('',(-0.35,0.35,-4.28626379701573E-17));
#11690=CARTESIAN_POINT('Origin',(0.,0.35,0.));
#11691=CARTESIAN_POINT('',(-0.325,0.375,-3.9801020972289E-17));
#11692=CARTESIAN_POINT('Origin',(0.,0.19,0.));
#11693=CARTESIAN_POINT('',(-0.35,0.03,-4.28626379701574E-17));
#11694=CARTESIAN_POINT('Origin',(0.,0.03,0.));
#11695=CARTESIAN_POINT('',(-0.35,0.19,-4.28626379701574E-17));
#11696=CARTESIAN_POINT('Origin',(0.,0.0149999999999999,0.));
#11697=CARTESIAN_POINT('',(-0.32,-3.29597460435593E-17,-3.91886975727153E-17));
#11698=CARTESIAN_POINT('Origin',(0.,0.,0.));
#11699=CARTESIAN_POINT('',(-0.335,0.0149999999999999,-4.10256677714363E-17));
#11700=CARTESIAN_POINT('Origin',(0.22,0.,0.));
#11701=CARTESIAN_POINT('',(-0.22,-6.93889390390723E-18,-2.69422295812418E-17));
#11702=CARTESIAN_POINT('Origin',(0.,0.,0.));
#11703=CARTESIAN_POINT('Origin',(0.,-0.02,0.));
#11704=CARTESIAN_POINT('',(-0.1954,-0.0492,2.39295984553393E-17));
#11705=CARTESIAN_POINT('Origin',(0.,-0.0492,0.));
#11706=CARTESIAN_POINT('',(-0.21,-0.02,-2.57175827820944E-17));
#11707=CARTESIAN_POINT('Origin',(0.,-0.8,0.));
#11708=CARTESIAN_POINT('',(-0.1954,-1.5646,2.39295984553393E-17));
#11709=CARTESIAN_POINT('Origin',(0.,-1.5646,0.));
#11710=CARTESIAN_POINT('',(-0.1954,-0.8,-2.39295984553393E-17));
#11711=CARTESIAN_POINT('Origin',(0.,-1.58,0.));
#11712=CARTESIAN_POINT('',(-0.16,-1.6,-1.95943487863577E-17));
#11713=CARTESIAN_POINT('Origin',(0.,-1.6,0.));
#11714=CARTESIAN_POINT('',(-0.18,-1.58,-2.20436423846524E-17));
#11715=CARTESIAN_POINT('Origin',(0.,-1.6,0.));
#11716=CARTESIAN_POINT('Origin',(0.0866025403784439,-0.4,-0.15));
#11717=CARTESIAN_POINT('',(0.173205080756888,-0.4,0.));
#11718=CARTESIAN_POINT('',(0.0866025403784439,-0.4,-0.15));
#11719=CARTESIAN_POINT('',(0.173205080756888,-0.4,0.));
#11720=CARTESIAN_POINT('',(0.0866025403784439,-0.64,-0.15));
#11721=CARTESIAN_POINT('',(0.0866025403784439,-0.4,-0.15));
#11722=CARTESIAN_POINT('',(0.173205080756888,-0.64,0.));
#11723=CARTESIAN_POINT('',(0.173205080756888,-0.64,0.));
#11724=CARTESIAN_POINT('',(0.173205080756888,-0.4,0.));
#11725=CARTESIAN_POINT('Origin',(-0.0866025403784438,-0.4,-0.15));
#11726=CARTESIAN_POINT('',(-0.0866025403784438,-0.4,-0.15));
#11727=CARTESIAN_POINT('',(0.0866025403784439,-0.4,-0.15));
#11728=CARTESIAN_POINT('',(-0.0866025403784438,-0.64,-0.15));
#11729=CARTESIAN_POINT('',(-0.0866025403784438,-0.4,-0.15));
#11730=CARTESIAN_POINT('',(0.0866025403784439,-0.64,-0.15));
#11731=CARTESIAN_POINT('Origin',(-0.173205080756888,-0.4,-2.77555756156289E-17));
#11732=CARTESIAN_POINT('',(-0.173205080756888,-0.4,-2.12115047744981E-17));
#11733=CARTESIAN_POINT('',(-0.0866025403784438,-0.4,-0.15));
#11734=CARTESIAN_POINT('',(-0.173205080756888,-0.64,-2.77555756156289E-17));
#11735=CARTESIAN_POINT('',(-0.173205080756888,-0.4,-2.12115047744981E-17));
#11736=CARTESIAN_POINT('',(-0.0866025403784438,-0.64,-0.15));
#11737=CARTESIAN_POINT('Origin',(-0.0866025403784439,-0.4,0.15));
#11738=CARTESIAN_POINT('',(-0.0866025403784439,-0.4,0.15));
#11739=CARTESIAN_POINT('',(-0.173205080756888,-0.4,-2.12115047744981E-17));
#11740=CARTESIAN_POINT('',(-0.0866025403784439,-0.64,0.15));
#11741=CARTESIAN_POINT('',(-0.0866025403784439,-0.4,0.15));
#11742=CARTESIAN_POINT('',(-0.173205080756888,-0.64,-2.12115047744981E-17));
#11743=CARTESIAN_POINT('Origin',(0.0866025403784439,-0.4,0.15));
#11744=CARTESIAN_POINT('',(0.0866025403784439,-0.4,0.15));
#11745=CARTESIAN_POINT('',(-0.0866025403784439,-0.4,0.15));
#11746=CARTESIAN_POINT('',(0.0866025403784439,-0.64,0.15));
#11747=CARTESIAN_POINT('',(0.0866025403784439,-0.4,0.15));
#11748=CARTESIAN_POINT('',(-0.0866025403784439,-0.64,0.15));
#11749=CARTESIAN_POINT('Origin',(0.173205080756888,-0.4,0.));
#11750=CARTESIAN_POINT('',(0.0866025403784439,-0.4,0.15));
#11751=CARTESIAN_POINT('',(0.0866025403784439,-0.64,0.15));
#11752=CARTESIAN_POINT('Origin',(0.,-0.4,-2.77555756156289E-17));
#11753=CARTESIAN_POINT('Origin',(0.,-0.64,-2.77555756156289E-17));
#12751=UNCERTAINTY_MEASURE_WITH_UNIT(LENGTH_MEASURE(0.001),#12805,
'DISTANCE_ACCURACY_VALUE',
'Maximum model space distance between geometric entities at asserted c
onnectivities');
#12768=UNCERTAINTY_MEASURE_WITH_UNIT(LENGTH_MEASURE(0.001),#12805,
'DISTANCE_ACCURACY_VALUE',
'Maximum model space distance between geometric entities at asserted c
onnectivities');
#12787=(
GEOMETRIC_REPRESENTATION_CONTEXT(3)
GLOBAL_UNCERTAINTY_ASSIGNED_CONTEXT((#12751))
GLOBAL_UNIT_ASSIGNED_CONTEXT((#12805,#12807,#12808))
REPRESENTATION_CONTEXT('','3D')
);
#12804=(
GEOMETRIC_REPRESENTATION_CONTEXT(3)
GLOBAL_UNCERTAINTY_ASSIGNED_CONTEXT((#12768))
GLOBAL_UNIT_ASSIGNED_CONTEXT((#12805,#12807,#12808))
REPRESENTATION_CONTEXT('','3D')
);
#12805=(
LENGTH_UNIT()
NAMED_UNIT(*)
SI_UNIT(.CENTI.,.METRE.)
);
#12807=(
NAMED_UNIT(*)
PLANE_ANGLE_UNIT()
SI_UNIT($,.RADIAN.)
);
#12808=(
NAMED_UNIT(*)
SI_UNIT($,.STERADIAN.)
SOLID_ANGLE_UNIT()
);
#12827=SHAPE_DEFINITION_REPRESENTATION(#12862,#13017);
#12862=PRODUCT_DEFINITION_SHAPE('',$,#13053);
#13017=SHAPE_REPRESENTATION('',(#8038),#12787);
#13034=PRODUCT_DEFINITION_CONTEXT('part definition',#13141,'design');
#13053=PRODUCT_DEFINITION('Cap Screw - M4x16','Cap Screw - M4x16',#13088,
#13034);
#13088=PRODUCT_DEFINITION_FORMATION('',$,#13161);
#13141=APPLICATION_CONTEXT(
'Core Data for Automotive Mechanical Design Process');
#13142=PRODUCT_CONTEXT('part definition',#13141,'mechanical');
#13161=PRODUCT('Cap Screw - M4x16','Cap Screw - M4x16',
'Cap Screw - M4x16',(#13142));
#13248=COLOUR_RGB('Black',0.12,0.14,0.17);
#13249=FILL_AREA_STYLE_COLOUR('',#13248);
#13250=FILL_AREA_STYLE('',(#13249));
#13251=SURFACE_STYLE_FILL_AREA(#13250);
#13252=SURFACE_SIDE_STYLE('',(#13251));
#13253=SURFACE_STYLE_USAGE(.BOTH.,#13252);
#13254=PRESENTATION_STYLE_ASSIGNMENT((#13253));
ENDSEC;
END-ISO-10303-21;
